ISO-10303-21;
HEADER;
/* Generated by software containing ST-Developer
 * from STEP Tools, Inc. (www.steptools.com) 
 */

FILE_DESCRIPTION(
/* description */ (''),
/* implementation_level */ '2;1');

FILE_NAME(
/* name */ 'Shaft.step',
/* time_stamp */ '2026-10-23T17:22:31+06:00',
/* author */ (''),
/* organization */ (''),
/* preprocessor_version */ 'ST-DEVELOPER v20.2',
/* originating_system */ 'Autodesk Translation Framework v15.15.0.0',
/* authorisation */ '');

FILE_SCHEMA (('AUTOMOTIVE_DESIGN { 1 0 10303 214 3 1 1 }'));
ENDSEC;

DATA;
#10=MECHANICAL_DESIGN_GEOMETRIC_PRESENTATION_REPRESENTATION('',(#85),#7315);
#65=SHAPE_REPRESENTATION_RELATIONSHIP('SRR','None',#7361,#75);
#75=ADVANCED_BREP_SHAPE_REPRESENTATION('',(#95),#7313);
#85=STYLED_ITEM('',(#7445),#95);
#95=MANIFOLD_SOLID_BREP('Shaft',#3222);
#386=LINE('',#7263,#546);
#546=VECTOR('',#4615,2.);
#686=CYLINDRICAL_SURFACE('',#3700,2.);
#724=PLANE('',#3703);
#725=PLANE('',#3704);
#903=FACE_OUTER_BOUND('',#1094,.T.);
#904=FACE_OUTER_BOUND('',#1095,.T.);
#905=FACE_OUTER_BOUND('',#1096,.T.);
#1094=EDGE_LOOP('',(#3010,#3011,#3012,#3013));
#1095=EDGE_LOOP('',(#3014));
#1096=EDGE_LOOP('',(#3015));
#1283=CIRCLE('',#3701,2.);
#1284=CIRCLE('',#3702,2.);
#1600=VERTEX_POINT('',#7260);
#1601=VERTEX_POINT('',#7262);
#2071=EDGE_CURVE('',#1600,#1600,#1283,.T.);
#2072=EDGE_CURVE('',#1600,#1601,#386,.T.);
#2073=EDGE_CURVE('',#1601,#1601,#1284,.T.);
#3010=ORIENTED_EDGE('',*,*,#2071,.F.);
#3011=ORIENTED_EDGE('',*,*,#2072,.T.);
#3012=ORIENTED_EDGE('',*,*,#2073,.T.);
#3013=ORIENTED_EDGE('',*,*,#2072,.F.);
#3014=ORIENTED_EDGE('',*,*,#2071,.T.);
#3015=ORIENTED_EDGE('',*,*,#2073,.F.);
#3207=ADVANCED_FACE('',(#903),#686,.T.);
#3208=ADVANCED_FACE('',(#904),#724,.T.);
#3209=ADVANCED_FACE('',(#905),#725,.F.);
#3222=CLOSED_SHELL('',(#3207,#3208,#3209));
#3699=AXIS2_PLACEMENT_3D('',#7258,#4609,#4610);
#3700=AXIS2_PLACEMENT_3D('',#7259,#4611,#4612);
#3701=AXIS2_PLACEMENT_3D('',#7261,#4613,#4614);
#3702=AXIS2_PLACEMENT_3D('',#7264,#4616,#4617);
#3703=AXIS2_PLACEMENT_3D('',#7265,#4618,#4619);
#3704=AXIS2_PLACEMENT_3D('',#7266,#4620,#4621);
#4609=DIRECTION('axis',(0.,0.,1.));
#4610=DIRECTION('refdir',(1.,0.,0.));
#4611=DIRECTION('center_axis',(1.,0.,0.));
#4612=DIRECTION('ref_axis',(0.,1.,0.));
#4613=DIRECTION('center_axis',(1.,0.,0.));
#4614=DIRECTION('ref_axis',(0.,1.,0.));
#4615=DIRECTION('',(-1.,0.,0.));
#4616=DIRECTION('center_axis',(1.,0.,0.));
#4617=DIRECTION('ref_axis',(0.,1.,0.));
#4618=DIRECTION('center_axis',(1.,0.,0.));
#4619=DIRECTION('ref_axis',(0.,1.,0.));
#4620=DIRECTION('center_axis',(1.,0.,0.));
#4621=DIRECTION('ref_axis',(0.,1.,0.));
#7258=CARTESIAN_POINT('',(0.,0.,0.));
#7259=CARTESIAN_POINT('Origin',(52.9998593353039,0.,0.));
#7260=CARTESIAN_POINT('',(57.9998593353039,-2.,-2.44929359829471E-16));
#7261=CARTESIAN_POINT('Origin',(57.9998593353039,0.,0.));
#7262=CARTESIAN_POINT('',(52.9998593353039,-2.,-2.44929359829471E-16));
#7263=CARTESIAN_POINT('',(52.9998593353039,-2.,-2.44929359829471E-16));
#7264=CARTESIAN_POINT('Origin',(52.9998593353039,0.,0.));
#7265=CARTESIAN_POINT('Origin',(57.9998593353039,0.,0.));
#7266=CARTESIAN_POINT('Origin',(52.9998593353039,0.,0.));
#7301=UNCERTAINTY_MEASURE_WITH_UNIT(LENGTH_MEASURE(0.01),#7316,
'DISTANCE_ACCURACY_VALUE',
'Maximum model space distance between geometric entities at asserted c
onnectivities');
#7303=UNCERTAINTY_MEASURE_WITH_UNIT(LENGTH_MEASURE(0.01),#7316,
'DISTANCE_ACCURACY_VALUE',
'Maximum model space distance between geometric entities at asserted c
onnectivities');
#7313=(
GEOMETRIC_REPRESENTATION_CONTEXT(3)
GLOBAL_UNCERTAINTY_ASSIGNED_CONTEXT((#7301))
GLOBAL_UNIT_ASSIGNED_CONTEXT((#7316,#7318,#7319))
REPRESENTATION_CONTEXT('','3D')
);
#7315=(
GEOMETRIC_REPRESENTATION_CONTEXT(3)
GLOBAL_UNCERTAINTY_ASSIGNED_CONTEXT((#7303))
GLOBAL_UNIT_ASSIGNED_CONTEXT((#7316,#7318,#7319))
REPRESENTATION_CONTEXT('','3D')
);
#7316=(
LENGTH_UNIT()
NAMED_UNIT(*)
SI_UNIT(.MILLI.,.METRE.)
);
#7318=(
NAMED_UNIT(*)
PLANE_ANGLE_UNIT()
SI_UNIT($,.RADIAN.)
);
#7319=(
NAMED_UNIT(*)
SI_UNIT($,.STERADIAN.)
SOLID_ANGLE_UNIT()
);
#7329=SHAPE_DEFINITION_REPRESENTATION(#7340,#7361);
#7340=PRODUCT_DEFINITION_SHAPE('',$,#7373);
#7361=SHAPE_REPRESENTATION('',(#3699),#7313);
#7363=PRODUCT_DEFINITION_CONTEXT('part definition',#7398,'design');
#7373=PRODUCT_DEFINITION('Shaft','Shaft',#7384,#7363);
#7384=PRODUCT_DEFINITION_FORMATION('',$,#7409);
#7398=APPLICATION_CONTEXT(
'Core Data for Automotive Mechanical Design Process');
#7399=PRODUCT_CONTEXT('part definition',#7398,'mechanical');
#7409=PRODUCT('Shaft','Shaft',$,(#7399));
#7439=COLOUR_RGB('Grey',0.48,0.52,0.57);
#7440=FILL_AREA_STYLE_COLOUR('',#7439);
#7441=FILL_AREA_STYLE('',(#7440));
#7442=SURFACE_STYLE_FILL_AREA(#7441);
#7443=SURFACE_SIDE_STYLE('',(#7442));
#7444=SURFACE_STYLE_USAGE(.BOTH.,#7443);
#7445=PRESENTATION_STYLE_ASSIGNMENT((#7444));
ENDSEC;
END-ISO-10303-21;
